ISO-10303-21;
HEADER;
/* Generated by software containing ST-Developer
 * from STEP Tools, Inc. (www.steptools.com) 
 */

FILE_DESCRIPTION(
/* description */ ('Line shaft on three pillow blocks'),
/* implementation_level */ '2;1');

FILE_NAME(
/* name */ 'Flat Washer - M6.step',
/* time_stamp */ '2026-10-27T10:49:19-07:00',
/* author */ (''),
/* organization */ (''),
/* preprocessor_version */ 'ST-DEVELOPER v20.2',
/* originating_system */ 'Autodesk Translation Framework v15.17.0.0',
/* authorisation */ '');

FILE_SCHEMA (('AUTOMOTIVE_DESIGN { 1 0 10303 214 3 1 1 }'));
ENDSEC;

DATA;
#10=MECHANICAL_DESIGN_GEOMETRIC_PRESENTATION_REPRESENTATION('',(#349),#8377);
#295=SHAPE_REPRESENTATION_RELATIONSHIP('SRR','None',#8510,#322);
#322=ADVANCED_BREP_SHAPE_REPRESENTATION('',(#377),#8359);
#349=STYLED_ITEM('',(#8725),#377);
#377=MANIFOLD_SOLID_BREP('Body1',#4335);
#427=FACE_BOUND('',#1017,.T.);
#428=FACE_BOUND('',#1019,.T.);
#534=PLANE('',#4797);
#535=PLANE('',#4798);
#726=FACE_OUTER_BOUND('',#1014,.T.);
#727=FACE_OUTER_BOUND('',#1015,.T.);
#728=FACE_OUTER_BOUND('',#1016,.T.);
#729=FACE_OUTER_BOUND('',#1018,.T.);
#1014=EDGE_LOOP('',(#3225,#3226,#3227,#3228));
#1015=EDGE_LOOP('',(#3229,#3230,#3231,#3232));
#1016=EDGE_LOOP('',(#3233));
#1017=EDGE_LOOP('',(#3234));
#1018=EDGE_LOOP('',(#3235));
#1019=EDGE_LOOP('',(#3236));
#1341=LINE('',#6785,#1668);
#1342=LINE('',#6791,#1669);
#1668=VECTOR('',#5514,0.32);
#1669=VECTOR('',#5521,0.6);
#1961=CIRCLE('',#4792,0.32);
#1962=CIRCLE('',#4793,0.32);
#1963=CIRCLE('',#4795,0.6);
#1964=CIRCLE('',#4796,0.6);
#2160=VERTEX_POINT('',#6782);
#2161=VERTEX_POINT('',#6784);
#2162=VERTEX_POINT('',#6788);
#2163=VERTEX_POINT('',#6790);
#2561=EDGE_CURVE('',#2160,#2160,#1961,.T.);
#2562=EDGE_CURVE('',#2160,#2161,#1341,.T.);
#2563=EDGE_CURVE('',#2161,#2161,#1962,.T.);
#2564=EDGE_CURVE('',#2162,#2162,#1963,.T.);
#2565=EDGE_CURVE('',#2162,#2163,#1342,.T.);
#2566=EDGE_CURVE('',#2163,#2163,#1964,.T.);
#3225=ORIENTED_EDGE('',*,*,#2561,.F.);
#3226=ORIENTED_EDGE('',*,*,#2562,.T.);
#3227=ORIENTED_EDGE('',*,*,#2563,.T.);
#3228=ORIENTED_EDGE('',*,*,#2562,.F.);
#3229=ORIENTED_EDGE('',*,*,#2564,.F.);
#3230=ORIENTED_EDGE('',*,*,#2565,.T.);
#3231=ORIENTED_EDGE('',*,*,#2566,.T.);
#3232=ORIENTED_EDGE('',*,*,#2565,.F.);
#3233=ORIENTED_EDGE('',*,*,#2564,.T.);
#3234=ORIENTED_EDGE('',*,*,#2561,.T.);
#3235=ORIENTED_EDGE('',*,*,#2566,.F.);
#3236=ORIENTED_EDGE('',*,*,#2563,.F.);
#4027=CYLINDRICAL_SURFACE('',#4791,0.32);
#4028=CYLINDRICAL_SURFACE('',#4794,0.6);
#4144=ADVANCED_FACE('',(#726),#4027,.F.);
#4145=ADVANCED_FACE('',(#727),#4028,.T.);
#4146=ADVANCED_FACE('',(#728,#427),#534,.T.);
#4147=ADVANCED_FACE('',(#729,#428),#535,.F.);
#4335=CLOSED_SHELL('',(#4144,#4145,#4146,#4147));
#4790=AXIS2_PLACEMENT_3D('',#6780,#5508,#5509);
#4791=AXIS2_PLACEMENT_3D('',#6781,#5510,#5511);
#4792=AXIS2_PLACEMENT_3D('',#6783,#5512,#5513);
#4793=AXIS2_PLACEMENT_3D('',#6786,#5515,#5516);
#4794=AXIS2_PLACEMENT_3D('',#6787,#5517,#5518);
#4795=AXIS2_PLACEMENT_3D('',#6789,#5519,#5520);
#4796=AXIS2_PLACEMENT_3D('',#6792,#5522,#5523);
#4797=AXIS2_PLACEMENT_3D('',#6793,#5524,#5525);
#4798=AXIS2_PLACEMENT_3D('',#6794,#5526,#5527);
#5508=DIRECTION('axis',(0.,0.,1.));
#5509=DIRECTION('refdir',(1.,0.,0.));
#5510=DIRECTION('center_axis',(0.,1.,0.));
#5511=DIRECTION('ref_axis',(1.,0.,0.));
#5512=DIRECTION('center_axis',(0.,-1.,0.));
#5513=DIRECTION('ref_axis',(1.,0.,0.));
#5514=DIRECTION('',(0.,-1.,0.));
#5515=DIRECTION('center_axis',(0.,-1.,0.));
#5516=DIRECTION('ref_axis',(1.,0.,0.));
#5517=DIRECTION('center_axis',(0.,1.,0.));
#5518=DIRECTION('ref_axis',(1.,0.,0.));
#5519=DIRECTION('center_axis',(0.,1.,0.));
#5520=DIRECTION('ref_axis',(1.,0.,0.));
#5521=DIRECTION('',(0.,-1.,0.));
#5522=DIRECTION('center_axis',(0.,1.,0.));
#5523=DIRECTION('ref_axis',(1.,0.,0.));
#5524=DIRECTION('center_axis',(0.,1.,0.));
#5525=DIRECTION('ref_axis',(1.,0.,0.));
#5526=DIRECTION('center_axis',(0.,1.,0.));
#5527=DIRECTION('ref_axis',(1.,0.,0.));
#6780=CARTESIAN_POINT('',(0.,0.,0.));
#6781=CARTESIAN_POINT('Origin',(0.,0.,0.));
#6782=CARTESIAN_POINT('',(-0.32,0.16,3.91886975727153E-17));
#6783=CARTESIAN_POINT('Origin',(0.,0.16,0.));
#6784=CARTESIAN_POINT('',(-0.32,0.,3.91886975727153E-17));
#6785=CARTESIAN_POINT('',(-0.32,0.,3.91886975727153E-17));
#6786=CARTESIAN_POINT('Origin',(0.,0.,0.));
#6787=CARTESIAN_POINT('Origin',(0.,0.,0.));
#6788=CARTESIAN_POINT('',(-0.6,0.16,7.34788079488412E-17));
#6789=CARTESIAN_POINT('Origin',(0.,0.16,0.));
#6790=CARTESIAN_POINT('',(-0.6,0.,7.34788079488412E-17));
#6791=CARTESIAN_POINT('',(-0.6,0.,7.34788079488412E-17));
#6792=CARTESIAN_POINT('Origin',(0.,0.,0.));
#6793=CARTESIAN_POINT('Origin',(0.,0.16,0.));
#6794=CARTESIAN_POINT('Origin',(0.,0.,0.));
#8327=UNCERTAINTY_MEASURE_WITH_UNIT(LENGTH_MEASURE(0.001),#8378,
'DISTANCE_ACCURACY_VALUE',
'Maximum model space distance between geometric entities at asserted c
onnectivities');
#8345=UNCERTAINTY_MEASURE_WITH_UNIT(LENGTH_MEASURE(0.001),#8378,
'DISTANCE_ACCURACY_VALUE',
'Maximum model space distance between geometric entities at asserted c
onnectivities');
#8359=(
GEOMETRIC_REPRESENTATION_CONTEXT(3)
GLOBAL_UNCERTAINTY_ASSIGNED_CONTEXT((#8327))
GLOBAL_UNIT_ASSIGNED_CONTEXT((#8378,#8380,#8381))
REPRESENTATION_CONTEXT('','3D')
);
#8377=(
GEOMETRIC_REPRESENTATION_CONTEXT(3)
GLOBAL_UNCERTAINTY_ASSIGNED_CONTEXT((#8345))
GLOBAL_UNIT_ASSIGNED_CONTEXT((#8378,#8380,#8381))
REPRESENTATION_CONTEXT('','3D')
);
#8378=(
LENGTH_UNIT()
NAMED_UNIT(*)
SI_UNIT(.CENTI.,.METRE.)
);
#8380=(
NAMED_UNIT(*)
PLANE_ANGLE_UNIT()
SI_UNIT($,.RADIAN.)
);
#8381=(
NAMED_UNIT(*)
SI_UNIT($,.STERADIAN.)
SOLID_ANGLE_UNIT()
);
#8395=SHAPE_DEFINITION_REPRESENTATION(#8426,#8510);
#8426=PRODUCT_DEFINITION_SHAPE('',$,#8542);
#8510=SHAPE_REPRESENTATION('',(#4790),#8359);
#8528=PRODUCT_DEFINITION_CONTEXT('part definition',#8623,'design');
#8542=PRODUCT_DEFINITION('Flat Washer - M6','Flat Washer - M6',#8573,#8528);
#8573=PRODUCT_DEFINITION_FORMATION('',$,#8638);
#8623=APPLICATION_CONTEXT(
'Core Data for Automotive Mechanical Design Process');
#8624=PRODUCT_CONTEXT('part definition',#8623,'mechanical');
#8638=PRODUCT('Flat Washer - M6','Flat Washer - M6','Flat Washer - M6',
(#8624));
#8719=COLOUR_RGB('Black',0.12,0.14,0.17);
#8720=FILL_AREA_STYLE_COLOUR('',#8719);
#8721=FILL_AREA_STYLE('',(#8720));
#8722=SURFACE_STYLE_FILL_AREA(#8721);
#8723=SURFACE_SIDE_STYLE('',(#8722));
#8724=SURFACE_STYLE_USAGE(.BOTH.,#8723);
#8725=PRESENTATION_STYLE_ASSIGNMENT((#8724));
ENDSEC;
END-ISO-10303-21;
